ISO-10303-21;
HEADER;
/* Generated by software containing ST-Developer
 * from STEP Tools, Inc. (www.steptools.com) 
 */

FILE_DESCRIPTION(
/* description */ ('Crank-driven oscillating fan base (mechanism only)'),

/* implementation_level */ '2;1');

FILE_NAME(
/* name */ 'Link bushing (1).step',
/* time_stamp */ '2026-10-28T03:25:00-07:00',
/* author */ (''),
/* organization */ (''),
/* preprocessor_version */ 'ST-DEVELOPER v20.2',
/* originating_system */ 'Autodesk Translation Framework v15.17.0.0',
/* authorisation */ '');

FILE_SCHEMA (('AUTOMOTIVE_DESIGN { 1 0 10303 214 3 1 1 }'));
ENDSEC;

DATA;
#10=MECHANICAL_DESIGN_GEOMETRIC_PRESENTATION_REPRESENTATION('',(#484),#11916);
#396=SHAPE_REPRESENTATION_RELATIONSHIP('SRR','None',#12124,#436);
#436=ADVANCED_BREP_SHAPE_REPRESENTATION('',(#529),#11915);
#484=STYLED_ITEM('',(#12361),#529);
#529=MANIFOLD_SOLID_BREP('Body1',#6117);
#690=FACE_BOUND('',#1795,.T.);
#691=FACE_BOUND('',#1797,.T.);
#884=PLANE('',#7402);
#885=PLANE('',#7403);
#1257=FACE_OUTER_BOUND('',#1792,.T.);
#1258=FACE_OUTER_BOUND('',#1793,.T.);
#1259=FACE_OUTER_BOUND('',#1794,.T.);
#1260=FACE_OUTER_BOUND('',#1796,.T.);
#1792=EDGE_LOOP('',(#5534,#5535,#5536,#5537));
#1793=EDGE_LOOP('',(#5538,#5539,#5540,#5541));
#1794=EDGE_LOOP('',(#5542));
#1795=EDGE_LOOP('',(#5543));
#1796=EDGE_LOOP('',(#5544));
#1797=EDGE_LOOP('',(#5545));
#2129=LINE('',#11806,#2462);
#2130=LINE('',#11812,#2463);
#2462=VECTOR('',#9420,0.305);
#2463=VECTOR('',#9427,0.5);
#2825=CIRCLE('',#7397,0.305);
#2826=CIRCLE('',#7398,0.305);
#2827=CIRCLE('',#7400,0.5);
#2828=CIRCLE('',#7401,0.5);
#3325=VERTEX_POINT('',#11803);
#3326=VERTEX_POINT('',#11805);
#3327=VERTEX_POINT('',#11809);
#3328=VERTEX_POINT('',#11811);
#4062=EDGE_CURVE('',#3325,#3325,#2825,.T.);
#4063=EDGE_CURVE('',#3325,#3326,#2129,.T.);
#4064=EDGE_CURVE('',#3326,#3326,#2826,.T.);
#4065=EDGE_CURVE('',#3327,#3327,#2827,.T.);
#4066=EDGE_CURVE('',#3327,#3328,#2130,.T.);
#4067=EDGE_CURVE('',#3328,#3328,#2828,.T.);
#5534=ORIENTED_EDGE('',*,*,#4062,.F.);
#5535=ORIENTED_EDGE('',*,*,#4063,.T.);
#5536=ORIENTED_EDGE('',*,*,#4064,.T.);
#5537=ORIENTED_EDGE('',*,*,#4063,.F.);
#5538=ORIENTED_EDGE('',*,*,#4065,.F.);
#5539=ORIENTED_EDGE('',*,*,#4066,.T.);
#5540=ORIENTED_EDGE('',*,*,#4067,.T.);
#5541=ORIENTED_EDGE('',*,*,#4066,.F.);
#5542=ORIENTED_EDGE('',*,*,#4065,.T.);
#5543=ORIENTED_EDGE('',*,*,#4062,.T.);
#5544=ORIENTED_EDGE('',*,*,#4067,.F.);
#5545=ORIENTED_EDGE('',*,*,#4064,.F.);
#5690=CYLINDRICAL_SURFACE('',#7396,0.305);
#5691=CYLINDRICAL_SURFACE('',#7399,0.5);
#6063=ADVANCED_FACE('',(#1257),#5690,.F.);
#6064=ADVANCED_FACE('',(#1258),#5691,.T.);
#6065=ADVANCED_FACE('',(#1259,#690),#884,.T.);
#6066=ADVANCED_FACE('',(#1260,#691),#885,.F.);
#6117=CLOSED_SHELL('',(#6063,#6064,#6065,#6066));
#7395=AXIS2_PLACEMENT_3D('',#11801,#9414,#9415);
#7396=AXIS2_PLACEMENT_3D('',#11802,#9416,#9417);
#7397=AXIS2_PLACEMENT_3D('',#11804,#9418,#9419);
#7398=AXIS2_PLACEMENT_3D('',#11807,#9421,#9422);
#7399=AXIS2_PLACEMENT_3D('',#11808,#9423,#9424);
#7400=AXIS2_PLACEMENT_3D('',#11810,#9425,#9426);
#7401=AXIS2_PLACEMENT_3D('',#11813,#9428,#9429);
#7402=AXIS2_PLACEMENT_3D('',#11814,#9430,#9431);
#7403=AXIS2_PLACEMENT_3D('',#11815,#9432,#9433);
#9414=DIRECTION('axis',(0.,0.,1.));
#9415=DIRECTION('refdir',(1.,0.,0.));
#9416=DIRECTION('center_axis',(0.,0.,1.));
#9417=DIRECTION('ref_axis',(1.,0.,0.));
#9418=DIRECTION('center_axis',(0.,0.,-1.));
#9419=DIRECTION('ref_axis',(1.,0.,0.));
#9420=DIRECTION('',(0.,0.,-1.));
#9421=DIRECTION('center_axis',(0.,0.,-1.));
#9422=DIRECTION('ref_axis',(1.,0.,0.));
#9423=DIRECTION('center_axis',(0.,0.,1.));
#9424=DIRECTION('ref_axis',(1.,0.,0.));
#9425=DIRECTION('center_axis',(0.,0.,1.));
#9426=DIRECTION('ref_axis',(1.,0.,0.));
#9427=DIRECTION('',(0.,0.,-1.));
#9428=DIRECTION('center_axis',(0.,0.,1.));
#9429=DIRECTION('ref_axis',(1.,0.,0.));
#9430=DIRECTION('center_axis',(0.,0.,1.));
#9431=DIRECTION('ref_axis',(1.,0.,0.));
#9432=DIRECTION('center_axis',(0.,0.,1.));
#9433=DIRECTION('ref_axis',(1.,0.,0.));
#11801=CARTESIAN_POINT('',(0.,0.,0.));
#11802=CARTESIAN_POINT('Origin',(8.,4.,8.6));
#11803=CARTESIAN_POINT('',(7.695,4.,9.4));
#11804=CARTESIAN_POINT('Origin',(8.,4.,9.4));
#11805=CARTESIAN_POINT('',(7.695,4.,8.6));
#11806=CARTESIAN_POINT('',(7.695,4.,8.6));
#11807=CARTESIAN_POINT('Origin',(8.,4.,8.6));
#11808=CARTESIAN_POINT('Origin',(8.,4.,8.6));
#11809=CARTESIAN_POINT('',(7.5,4.,9.4));
#11810=CARTESIAN_POINT('Origin',(8.,4.,9.4));
#11811=CARTESIAN_POINT('',(7.5,4.,8.6));
#11812=CARTESIAN_POINT('',(7.5,4.,8.6));
#11813=CARTESIAN_POINT('Origin',(8.,4.,8.6));
#11814=CARTESIAN_POINT('Origin',(8.,4.,9.4));
#11815=CARTESIAN_POINT('Origin',(8.,4.,8.6));
#11868=UNCERTAINTY_MEASURE_WITH_UNIT(LENGTH_MEASURE(0.001),#11917,
'DISTANCE_ACCURACY_VALUE',
'Maximum model space distance between geometric entities at asserted c
onnectivities');
#11869=UNCERTAINTY_MEASURE_WITH_UNIT(LENGTH_MEASURE(0.001),#11917,
'DISTANCE_ACCURACY_VALUE',
'Maximum model space distance between geometric entities at asserted c
onnectivities');
#11915=(
GEOMETRIC_REPRESENTATION_CONTEXT(3)
GLOBAL_UNCERTAINTY_ASSIGNED_CONTEXT((#11868))
GLOBAL_UNIT_ASSIGNED_CONTEXT((#11917,#11919,#11920))
REPRESENTATION_CONTEXT('','3D')
);
#11916=(
GEOMETRIC_REPRESENTATION_CONTEXT(3)
GLOBAL_UNCERTAINTY_ASSIGNED_CONTEXT((#11869))
GLOBAL_UNIT_ASSIGNED_CONTEXT((#11917,#11919,#11920))
REPRESENTATION_CONTEXT('','3D')
);
#11917=(
LENGTH_UNIT()
NAMED_UNIT(*)
SI_UNIT(.CENTI.,.METRE.)
);
#11919=(
NAMED_UNIT(*)
PLANE_ANGLE_UNIT()
SI_UNIT($,.RADIAN.)
);
#11920=(
NAMED_UNIT(*)
SI_UNIT($,.STERADIAN.)
SOLID_ANGLE_UNIT()
);
#11966=SHAPE_DEFINITION_REPRESENTATION(#12071,#12124);
#12071=PRODUCT_DEFINITION_SHAPE('',$,#12171);
#12124=SHAPE_REPRESENTATION('',(#7395),#11915);
#12125=PRODUCT_DEFINITION_CONTEXT('part definition',#12265,'design');
#12171=PRODUCT_DEFINITION('Link bushing (1)','Link bushing (1)',#12217,#12125);
#12217=PRODUCT_DEFINITION_FORMATION('',$,#12312);
#12265=APPLICATION_CONTEXT(
'Core Data for Automotive Mechanical Design Process');
#12266=PRODUCT_CONTEXT('part definition',#12265,'mechanical');
#12312=PRODUCT('Link bushing (1)','Link bushing (1)','Link bushing (1)',(#12266));
#12355=COLOUR_RGB('Light Blue',0.38,0.62,0.78);
#12356=FILL_AREA_STYLE_COLOUR('',#12355);
#12357=FILL_AREA_STYLE('',(#12356));
#12358=SURFACE_STYLE_FILL_AREA(#12357);
#12359=SURFACE_SIDE_STYLE('',(#12358));
#12360=SURFACE_STYLE_USAGE(.BOTH.,#12359);
#12361=PRESENTATION_STYLE_ASSIGNMENT((#12360));
ENDSEC;
END-ISO-10303-21;
